ISO-10303-21;
HEADER;
/* Generated by software containing ST-Developer
 * from STEP Tools, Inc. (www.steptools.com) 
 */

FILE_DESCRIPTION(
/* description */ (''),
/* implementation_level */ '2;1');

FILE_NAME(
/* name */ 'Front_part.step',
/* time_stamp */ '2026-10-22T16:03:28+06:00',
/* author */ (''),
/* organization */ (''),
/* preprocessor_version */ 'ST-DEVELOPER v20.2',
/* originating_system */ 'Autodesk Translation Framework v15.15.0.0',
/* authorisation */ '');

FILE_SCHEMA (('AUTOMOTIVE_DESIGN { 1 0 10303 214 3 1 1 }'));
ENDSEC;

DATA;
#10=MECHANICAL_DESIGN_GEOMETRIC_PRESENTATION_REPRESENTATION('',(#90),#6096);
#57=TOROIDAL_SURFACE('',#3904,33.837899857748,2.);
#58=TOROIDAL_SURFACE('',#3912,15.946575006305,2.);
#59=TOROIDAL_SURFACE('',#3920,11.946575006305,2.);
#60=TOROIDAL_SURFACE('',#3924,29.837899857748,2.);
#61=TOROIDAL_SURFACE('',#3926,34.8878705819456,2.);
#68=SHAPE_REPRESENTATION_RELATIONSHIP('SRR','None',#6143,#79);
#79=ADVANCED_BREP_SHAPE_REPRESENTATION('',(#101),#6091);
#90=STYLED_ITEM('',(#6248),#101);
#101=MANIFOLD_SOLID_BREP('Front_part',#3599);
#124=FACE_BOUND('',#619,.T.);
#125=FACE_BOUND('',#623,.T.);
#246=PLANE('',#3910);
#247=PLANE('',#3918);
#248=PLANE('',#3923);
#249=PLANE('',#3931);
#410=FACE_OUTER_BOUND('',#616,.T.);
#411=FACE_OUTER_BOUND('',#617,.T.);
#412=FACE_OUTER_BOUND('',#618,.T.);
#413=FACE_OUTER_BOUND('',#620,.T.);
#414=FACE_OUTER_BOUND('',#621,.T.);
#415=FACE_OUTER_BOUND('',#622,.T.);
#416=FACE_OUTER_BOUND('',#624,.T.);
#417=FACE_OUTER_BOUND('',#625,.T.);
#418=FACE_OUTER_BOUND('',#626,.T.);
#419=FACE_OUTER_BOUND('',#627,.T.);
#420=FACE_OUTER_BOUND('',#628,.T.);
#421=FACE_OUTER_BOUND('',#629,.T.);
#616=EDGE_LOOP('',(#2990,#2991,#2992,#2993));
#617=EDGE_LOOP('',(#2994,#2995,#2996,#2997));
#618=EDGE_LOOP('',(#2998));
#619=EDGE_LOOP('',(#2999));
#620=EDGE_LOOP('',(#3000,#3001,#3002,#3003));
#621=EDGE_LOOP('',(#3004,#3005,#3006,#3007));
#622=EDGE_LOOP('',(#3008));
#623=EDGE_LOOP('',(#3009));
#624=EDGE_LOOP('',(#3010,#3011,#3012,#3013));
#625=EDGE_LOOP('',(#3014));
#626=EDGE_LOOP('',(#3015,#3016,#3017,#3018));
#627=EDGE_LOOP('',(#3019,#3020,#3021,#3022));
#628=EDGE_LOOP('',(#3023,#3024,#3025,#3026));
#629=EDGE_LOOP('',(#3027));
#966=LINE('',#5679,#1345);
#967=LINE('',#5692,#1346);
#968=LINE('',#5709,#1347);
#1345=VECTOR('',#4651,31.837899857748);
#1346=VECTOR('',#4668,13.946575006305);
#1347=VECTOR('',#4693,36.8878705819456);
#1542=CIRCLE('',#3905,33.837899857748);
#1543=CIRCLE('',#3906,2.);
#1544=CIRCLE('',#3907,31.837899857748);
#1545=CIRCLE('',#3909,31.837899857748);
#1546=CIRCLE('',#3911,34.8878705819456);
#1547=CIRCLE('',#3913,15.946575006305);
#1548=CIRCLE('',#3914,2.);
#1549=CIRCLE('',#3915,13.946575006305);
#1550=CIRCLE('',#3917,13.946575006305);
#1551=CIRCLE('',#3919,29.837899857748);
#1552=CIRCLE('',#3921,11.946575006305);
#1553=CIRCLE('',#3922,2.);
#1554=CIRCLE('',#3925,2.);
#1555=CIRCLE('',#3927,2.);
#1556=CIRCLE('',#3928,36.8878705819456);
#1557=CIRCLE('',#3930,36.8878705819456);
#1786=VERTEX_POINT('',#5671);
#1787=VERTEX_POINT('',#5673);
#1788=VERTEX_POINT('',#5677);
#1789=VERTEX_POINT('',#5681);
#1790=VERTEX_POINT('',#5684);
#1791=VERTEX_POINT('',#5686);
#1792=VERTEX_POINT('',#5690);
#1793=VERTEX_POINT('',#5694);
#1794=VERTEX_POINT('',#5697);
#1795=VERTEX_POINT('',#5704);
#1796=VERTEX_POINT('',#5708);
#2207=EDGE_CURVE('',#1786,#1786,#1542,.T.);
#2208=EDGE_CURVE('',#1786,#1787,#1543,.T.);
#2209=EDGE_CURVE('',#1787,#1787,#1544,.T.);
#2210=EDGE_CURVE('',#1788,#1788,#1545,.T.);
#2211=EDGE_CURVE('',#1788,#1787,#966,.T.);
#2212=EDGE_CURVE('',#1789,#1789,#1546,.T.);
#2213=EDGE_CURVE('',#1790,#1790,#1547,.T.);
#2214=EDGE_CURVE('',#1790,#1791,#1548,.T.);
#2215=EDGE_CURVE('',#1791,#1791,#1549,.T.);
#2216=EDGE_CURVE('',#1792,#1792,#1550,.T.);
#2217=EDGE_CURVE('',#1792,#1791,#967,.T.);
#2218=EDGE_CURVE('',#1793,#1793,#1551,.T.);
#2219=EDGE_CURVE('',#1794,#1794,#1552,.T.);
#2220=EDGE_CURVE('',#1794,#1792,#1553,.T.);
#2221=EDGE_CURVE('',#1793,#1788,#1554,.T.);
#2222=EDGE_CURVE('',#1789,#1795,#1555,.T.);
#2223=EDGE_CURVE('',#1795,#1795,#1556,.T.);
#2224=EDGE_CURVE('',#1795,#1796,#968,.T.);
#2225=EDGE_CURVE('',#1796,#1796,#1557,.T.);
#2990=ORIENTED_EDGE('',*,*,#2207,.T.);
#2991=ORIENTED_EDGE('',*,*,#2208,.T.);
#2992=ORIENTED_EDGE('',*,*,#2209,.T.);
#2993=ORIENTED_EDGE('',*,*,#2208,.F.);
#2994=ORIENTED_EDGE('',*,*,#2210,.F.);
#2995=ORIENTED_EDGE('',*,*,#2211,.T.);
#2996=ORIENTED_EDGE('',*,*,#2209,.F.);
#2997=ORIENTED_EDGE('',*,*,#2211,.F.);
#2998=ORIENTED_EDGE('',*,*,#2212,.F.);
#2999=ORIENTED_EDGE('',*,*,#2207,.F.);
#3000=ORIENTED_EDGE('',*,*,#2213,.T.);
#3001=ORIENTED_EDGE('',*,*,#2214,.T.);
#3002=ORIENTED_EDGE('',*,*,#2215,.T.);
#3003=ORIENTED_EDGE('',*,*,#2214,.F.);
#3004=ORIENTED_EDGE('',*,*,#2216,.F.);
#3005=ORIENTED_EDGE('',*,*,#2217,.T.);
#3006=ORIENTED_EDGE('',*,*,#2215,.F.);
#3007=ORIENTED_EDGE('',*,*,#2217,.F.);
#3008=ORIENTED_EDGE('',*,*,#2218,.F.);
#3009=ORIENTED_EDGE('',*,*,#2213,.F.);
#3010=ORIENTED_EDGE('',*,*,#2219,.T.);
#3011=ORIENTED_EDGE('',*,*,#2220,.T.);
#3012=ORIENTED_EDGE('',*,*,#2216,.T.);
#3013=ORIENTED_EDGE('',*,*,#2220,.F.);
#3014=ORIENTED_EDGE('',*,*,#2219,.F.);
#3015=ORIENTED_EDGE('',*,*,#2218,.T.);
#3016=ORIENTED_EDGE('',*,*,#2221,.T.);
#3017=ORIENTED_EDGE('',*,*,#2210,.T.);
#3018=ORIENTED_EDGE('',*,*,#2221,.F.);
#3019=ORIENTED_EDGE('',*,*,#2212,.T.);
#3020=ORIENTED_EDGE('',*,*,#2222,.T.);
#3021=ORIENTED_EDGE('',*,*,#2223,.T.);
#3022=ORIENTED_EDGE('',*,*,#2222,.F.);
#3023=ORIENTED_EDGE('',*,*,#2223,.F.);
#3024=ORIENTED_EDGE('',*,*,#2224,.T.);
#3025=ORIENTED_EDGE('',*,*,#2225,.T.);
#3026=ORIENTED_EDGE('',*,*,#2224,.F.);
#3027=ORIENTED_EDGE('',*,*,#2225,.F.);
#3386=CYLINDRICAL_SURFACE('',#3908,31.837899857748);
#3387=CYLINDRICAL_SURFACE('',#3916,13.946575006305);
#3388=CYLINDRICAL_SURFACE('',#3929,36.8878705819456);
#3517=ADVANCED_FACE('',(#410),#57,.F.);
#3518=ADVANCED_FACE('',(#411),#3386,.T.);
#3519=ADVANCED_FACE('',(#412,#124),#246,.T.);
#3520=ADVANCED_FACE('',(#413),#58,.F.);
#3521=ADVANCED_FACE('',(#414),#3387,.T.);
#3522=ADVANCED_FACE('',(#415,#125),#247,.T.);
#3523=ADVANCED_FACE('',(#416),#59,.T.);
#3524=ADVANCED_FACE('',(#417),#248,.T.);
#3525=ADVANCED_FACE('',(#418),#60,.T.);
#3526=ADVANCED_FACE('',(#419),#61,.T.);
#3527=ADVANCED_FACE('',(#420),#3388,.T.);
#3528=ADVANCED_FACE('',(#421),#249,.T.);
#3599=CLOSED_SHELL('',(#3517,#3518,#3519,#3520,#3521,#3522,#3523,#3524,
#3525,#3526,#3527,#3528));
#3903=AXIS2_PLACEMENT_3D('',#5669,#4637,#4638);
#3904=AXIS2_PLACEMENT_3D('',#5670,#4639,#4640);
#3905=AXIS2_PLACEMENT_3D('',#5672,#4641,#4642);
#3906=AXIS2_PLACEMENT_3D('',#5674,#4643,#4644);
#3907=AXIS2_PLACEMENT_3D('',#5675,#4645,#4646);
#3908=AXIS2_PLACEMENT_3D('',#5676,#4647,#4648);
#3909=AXIS2_PLACEMENT_3D('',#5678,#4649,#4650);
#3910=AXIS2_PLACEMENT_3D('',#5680,#4652,#4653);
#3911=AXIS2_PLACEMENT_3D('',#5682,#4654,#4655);
#3912=AXIS2_PLACEMENT_3D('',#5683,#4656,#4657);
#3913=AXIS2_PLACEMENT_3D('',#5685,#4658,#4659);
#3914=AXIS2_PLACEMENT_3D('',#5687,#4660,#4661);
#3915=AXIS2_PLACEMENT_3D('',#5688,#4662,#4663);
#3916=AXIS2_PLACEMENT_3D('',#5689,#4664,#4665);
#3917=AXIS2_PLACEMENT_3D('',#5691,#4666,#4667);
#3918=AXIS2_PLACEMENT_3D('',#5693,#4669,#4670);
#3919=AXIS2_PLACEMENT_3D('',#5695,#4671,#4672);
#3920=AXIS2_PLACEMENT_3D('',#5696,#4673,#4674);
#3921=AXIS2_PLACEMENT_3D('',#5698,#4675,#4676);
#3922=AXIS2_PLACEMENT_3D('',#5699,#4677,#4678);
#3923=AXIS2_PLACEMENT_3D('',#5700,#4679,#4680);
#3924=AXIS2_PLACEMENT_3D('',#5701,#4681,#4682);
#3925=AXIS2_PLACEMENT_3D('',#5702,#4683,#4684);
#3926=AXIS2_PLACEMENT_3D('',#5703,#4685,#4686);
#3927=AXIS2_PLACEMENT_3D('',#5705,#4687,#4688);
#3928=AXIS2_PLACEMENT_3D('',#5706,#4689,#4690);
#3929=AXIS2_PLACEMENT_3D('',#5707,#4691,#4692);
#3930=AXIS2_PLACEMENT_3D('',#5710,#4694,#4695);
#3931=AXIS2_PLACEMENT_3D('',#5711,#4696,#4697);
#4637=DIRECTION('axis',(0.,0.,1.));
#4638=DIRECTION('refdir',(1.,0.,0.));
#4639=DIRECTION('center_axis',(0.,-1.,0.));
#4640=DIRECTION('ref_axis',(0.,0.,-1.));
#4641=DIRECTION('center_axis',(0.,-1.,0.));
#4642=DIRECTION('ref_axis',(0.,0.,1.));
#4643=DIRECTION('center_axis',(-1.,0.,-1.22464679914735E-16));
#4644=DIRECTION('ref_axis',(-1.22464679914735E-16,0.,1.));
#4645=DIRECTION('center_axis',(0.,1.,0.));
#4646=DIRECTION('ref_axis',(0.,0.,1.));
#4647=DIRECTION('center_axis',(0.,-1.,0.));
#4648=DIRECTION('ref_axis',(0.,0.,-1.));
#4649=DIRECTION('center_axis',(0.,-1.,0.));
#4650=DIRECTION('ref_axis',(0.,0.,1.));
#4651=DIRECTION('',(0.,1.,0.));
#4652=DIRECTION('center_axis',(0.,-1.,0.));
#4653=DIRECTION('ref_axis',(0.,0.,-1.));
#4654=DIRECTION('center_axis',(0.,1.,0.));
#4655=DIRECTION('ref_axis',(1.20388952477896E-16,0.,1.));
#4656=DIRECTION('center_axis',(0.,-1.,0.));
#4657=DIRECTION('ref_axis',(0.,0.,-1.));
#4658=DIRECTION('center_axis',(0.,-1.,0.));
#4659=DIRECTION('ref_axis',(0.,0.,1.));
#4660=DIRECTION('center_axis',(-1.,0.,-1.22464679914735E-16));
#4661=DIRECTION('ref_axis',(-1.22464679914735E-16,0.,1.));
#4662=DIRECTION('center_axis',(0.,1.,0.));
#4663=DIRECTION('ref_axis',(0.,0.,1.));
#4664=DIRECTION('center_axis',(0.,-1.,0.));
#4665=DIRECTION('ref_axis',(0.,0.,-1.));
#4666=DIRECTION('center_axis',(0.,-1.,0.));
#4667=DIRECTION('ref_axis',(0.,0.,1.));
#4668=DIRECTION('',(0.,1.,0.));
#4669=DIRECTION('center_axis',(0.,-1.,0.));
#4670=DIRECTION('ref_axis',(0.,0.,-1.));
#4671=DIRECTION('center_axis',(0.,1.,0.));
#4672=DIRECTION('ref_axis',(0.,0.,1.));
#4673=DIRECTION('center_axis',(0.,-1.,0.));
#4674=DIRECTION('ref_axis',(0.,0.,-1.));
#4675=DIRECTION('center_axis',(0.,1.,0.));
#4676=DIRECTION('ref_axis',(0.,0.,1.));
#4677=DIRECTION('center_axis',(-1.,0.,-1.22464679914735E-16));
#4678=DIRECTION('ref_axis',(-1.22464679914735E-16,0.,1.));
#4679=DIRECTION('center_axis',(0.,-1.,0.));
#4680=DIRECTION('ref_axis',(0.,0.,-1.));
#4681=DIRECTION('center_axis',(0.,-1.,0.));
#4682=DIRECTION('ref_axis',(0.,0.,-1.));
#4683=DIRECTION('center_axis',(-1.,0.,-1.22464679914735E-16));
#4684=DIRECTION('ref_axis',(-1.22464679914735E-16,0.,1.));
#4685=DIRECTION('center_axis',(0.,-1.,0.));
#4686=DIRECTION('ref_axis',(0.,0.,-1.));
#4687=DIRECTION('center_axis',(-1.,0.,-1.22464679914735E-16));
#4688=DIRECTION('ref_axis',(-1.22464679914735E-16,0.,1.));
#4689=DIRECTION('center_axis',(0.,-1.,0.));
#4690=DIRECTION('ref_axis',(1.20388952477896E-16,0.,1.));
#4691=DIRECTION('center_axis',(0.,-1.,0.));
#4692=DIRECTION('ref_axis',(0.,0.,-1.));
#4693=DIRECTION('',(0.,1.,0.));
#4694=DIRECTION('center_axis',(0.,-1.,0.));
#4695=DIRECTION('ref_axis',(1.,0.,0.));
#4696=DIRECTION('center_axis',(0.,1.,0.));
#4697=DIRECTION('ref_axis',(0.,0.,1.));
#5669=CARTESIAN_POINT('',(0.,0.,0.));
#5670=CARTESIAN_POINT('Origin',(4.44089209850063E-15,22.3469309188597,41.5000000000007));
#5671=CARTESIAN_POINT('',(2.96944523434646E-16,24.3469309188597,75.3378998577488));
#5672=CARTESIAN_POINT('Origin',(4.44089209850063E-15,24.3469309188597,41.5000000000007));
#5673=CARTESIAN_POINT('',(5.41873883264117E-16,22.3469309188597,73.3378998577488));
#5674=CARTESIAN_POINT('Origin',(2.96944523434646E-16,22.3469309188597,75.3378998577488));
#5675=CARTESIAN_POINT('Origin',(4.44089209850063E-15,22.3469309188597,41.5000000000007));
#5676=CARTESIAN_POINT('Origin',(4.44089209850063E-15,19.2969601946621,41.5000000000007));
#5677=CARTESIAN_POINT('',(5.41873883264117E-16,16.2469894704645,73.3378998577488));
#5678=CARTESIAN_POINT('Origin',(4.44089209850063E-15,16.2469894704645,41.5000000000007));
#5679=CARTESIAN_POINT('',(5.41873883264117E-16,19.2969601946621,73.3378998577488));
#5680=CARTESIAN_POINT('Origin',(4.44089209850063E-15,24.3469309188597,9.66210014225272));
#5681=CARTESIAN_POINT('',(1.68360194775942E-16,24.3469309188597,76.3878705819464));
#5682=CARTESIAN_POINT('Origin',(4.44089209850063E-15,24.3469309188597,41.5000000000007));
#5683=CARTESIAN_POINT('Origin',(4.44089209850063E-15,12.2469894704645,41.5000000000007));
#5684=CARTESIAN_POINT('',(2.48799989461716E-15,14.2469894704645,57.4465750063058));
#5685=CARTESIAN_POINT('Origin',(4.44089209850063E-15,14.2469894704645,41.5000000000007));
#5686=CARTESIAN_POINT('',(2.73292925444663E-15,12.2469894704645,55.4465750063058));
#5687=CARTESIAN_POINT('Origin',(2.48799989461716E-15,12.2469894704645,57.4465750063058));
#5688=CARTESIAN_POINT('Origin',(4.44089209850063E-15,12.2469894704645,41.5000000000007));
#5689=CARTESIAN_POINT('Origin',(4.44089209850063E-15,7.53774265117334,41.5000000000007));
#5690=CARTESIAN_POINT('',(2.73292925444663E-15,2.82849583188222,55.4465750063058));
#5691=CARTESIAN_POINT('Origin',(4.44089209850063E-15,2.82849583188222,41.5000000000007));
#5692=CARTESIAN_POINT('',(2.73292925444663E-15,7.53774265117334,55.4465750063058));
#5693=CARTESIAN_POINT('Origin',(4.44089209850063E-15,14.2469894704645,27.5534249936957));
#5694=CARTESIAN_POINT('',(7.86803243093589E-16,14.2469894704645,71.3378998577488));
#5695=CARTESIAN_POINT('Origin',(4.44089209850063E-15,14.2469894704645,41.5000000000007));
#5696=CARTESIAN_POINT('Origin',(4.44089209850063E-15,2.82849583188222,41.5000000000007));
#5697=CARTESIAN_POINT('',(2.9778586142761E-15,0.828495831882226,53.4465750063058));
#5698=CARTESIAN_POINT('Origin',(4.44089209850063E-15,0.828495831882226,
41.5000000000007));
#5699=CARTESIAN_POINT('Origin',(2.9778586142761E-15,2.82849583188222,53.4465750063058));
#5700=CARTESIAN_POINT('Origin',(4.44089209850063E-15,0.828495831882226,
41.5000000000007));
#5701=CARTESIAN_POINT('Origin',(4.44089209850063E-15,16.2469894704645,41.5000000000007));
#5702=CARTESIAN_POINT('Origin',(7.86803243093589E-16,16.2469894704645,71.3378998577488));
#5703=CARTESIAN_POINT('Origin',(4.44089209850063E-15,26.3469309188597,41.5000000000007));
#5704=CARTESIAN_POINT('',(-7.65691650535287E-17,26.3469309188597,78.3878705819464));
#5705=CARTESIAN_POINT('Origin',(1.68360194775942E-16,26.3469309188597,76.3878705819464));
#5706=CARTESIAN_POINT('Origin',(4.44089209850063E-15,26.3469309188597,41.5000000000007));
#5707=CARTESIAN_POINT('Origin',(4.44089209850063E-15,30.673456552356,41.5000000000007));
#5708=CARTESIAN_POINT('',(-7.65691650535287E-17,36.9999821858522,78.3878705819464));
#5709=CARTESIAN_POINT('',(-7.65691650535287E-17,30.673456552356,78.3878705819464));
#5710=CARTESIAN_POINT('Origin',(4.44089209850063E-15,36.9999821858522,41.5000000000007));
#5711=CARTESIAN_POINT('Origin',(4.44089209850063E-15,36.9999821858522,4.6121294180551));
#6078=UNCERTAINTY_MEASURE_WITH_UNIT(LENGTH_MEASURE(0.01),#6097,
'DISTANCE_ACCURACY_VALUE',
'Maximum model space distance between geometric entities at asserted c
onnectivities');
#6083=UNCERTAINTY_MEASURE_WITH_UNIT(LENGTH_MEASURE(0.01),#6097,
'DISTANCE_ACCURACY_VALUE',
'Maximum model space distance between geometric entities at asserted c
onnectivities');
#6091=(
GEOMETRIC_REPRESENTATION_CONTEXT(3)
GLOBAL_UNCERTAINTY_ASSIGNED_CONTEXT((#6078))
GLOBAL_UNIT_ASSIGNED_CONTEXT((#6097,#6099,#6100))
REPRESENTATION_CONTEXT('','3D')
);
#6096=(
GEOMETRIC_REPRESENTATION_CONTEXT(3)
GLOBAL_UNCERTAINTY_ASSIGNED_CONTEXT((#6083))
GLOBAL_UNIT_ASSIGNED_CONTEXT((#6097,#6099,#6100))
REPRESENTATION_CONTEXT('','3D')
);
#6097=(
LENGTH_UNIT()
NAMED_UNIT(*)
SI_UNIT(.MILLI.,.METRE.)
);
#6099=(
NAMED_UNIT(*)
PLANE_ANGLE_UNIT()
SI_UNIT($,.RADIAN.)
);
#6100=(
NAMED_UNIT(*)
SI_UNIT($,.STERADIAN.)
SOLID_ANGLE_UNIT()
);
#6108=SHAPE_DEFINITION_REPRESENTATION(#6120,#6143);
#6120=PRODUCT_DEFINITION_SHAPE('',$,#6156);
#6143=SHAPE_REPRESENTATION('',(#3903),#6091);
#6148=PRODUCT_DEFINITION_CONTEXT('part definition',#6186,'design');
#6156=PRODUCT_DEFINITION('Front_part','Front_part',#6168,#6148);
#6168=PRODUCT_DEFINITION_FORMATION('',$,#6195);
#6186=APPLICATION_CONTEXT(
'Core Data for Automotive Mechanical Design Process');
#6187=PRODUCT_CONTEXT('part definition',#6186,'mechanical');
#6195=PRODUCT('Front_part','Front_part',$,(#6187));
#6242=COLOUR_RGB('Sky Blue',0.24,0.69,0.87);
#6243=FILL_AREA_STYLE_COLOUR('',#6242);
#6244=FILL_AREA_STYLE('',(#6243));
#6245=SURFACE_STYLE_FILL_AREA(#6244);
#6246=SURFACE_SIDE_STYLE('',(#6245));
#6247=SURFACE_STYLE_USAGE(.BOTH.,#6246);
#6248=PRESENTATION_STYLE_ASSIGNMENT((#6247));
ENDSEC;
END-ISO-10303-21;
